ISO-10303-21;
HEADER;
/* Generated by software containing ST-Developer
 * from STEP Tools, Inc. (www.steptools.com) 
 */

FILE_DESCRIPTION(
/* description */ ('Dual-rail gantry carriage'),
/* implementation_level */ '2;1');

FILE_NAME(
/* name */ 'Flat Washer - M5.step',
/* time_stamp */ '2026-10-27T10:49:15-07:00',
/* author */ (''),
/* organization */ (''),
/* preprocessor_version */ 'ST-DEVELOPER v20.2',
/* originating_system */ 'Autodesk Translation Framework v15.17.0.0',
/* authorisation */ '');

FILE_SCHEMA (('AUTOMOTIVE_DESIGN { 1 0 10303 214 3 1 1 }'));
ENDSEC;

DATA;
#10=MECHANICAL_DESIGN_GEOMETRIC_PRESENTATION_REPRESENTATION('',(#610),#12804);
#505=CONICAL_SURFACE('',#8264,0.275,0.785398163397449);
#548=SHAPE_REPRESENTATION_RELATIONSHIP('SRR','None',#13028,#579);
#579=ADVANCED_BREP_SHAPE_REPRESENTATION('',(#639),#12798);
#610=STYLED_ITEM('',(#13254),#639);
#639=MANIFOLD_SOLID_BREP('Body1',#7390);
#755=FACE_BOUND('',#1878,.T.);
#756=FACE_BOUND('',#1881,.T.);
#1009=PLANE('',#8269);
#1010=PLANE('',#8273);
#1373=FACE_OUTER_BOUND('',#1875,.T.);
#1374=FACE_OUTER_BOUND('',#1876,.T.);
#1375=FACE_OUTER_BOUND('',#1877,.T.);
#1376=FACE_OUTER_BOUND('',#1879,.T.);
#1377=FACE_OUTER_BOUND('',#1880,.T.);
#1875=EDGE_LOOP('',(#6657,#6658,#6659,#6660));
#1876=EDGE_LOOP('',(#6661,#6662,#6663,#6664));
#1877=EDGE_LOOP('',(#6665));
#1878=EDGE_LOOP('',(#6666));
#1879=EDGE_LOOP('',(#6667,#6668,#6669,#6670));
#1880=EDGE_LOOP('',(#6671));
#1881=EDGE_LOOP('',(#6672));
#2578=LINE('',#12362,#3287);
#2579=LINE('',#12366,#3288);
#2580=LINE('',#12373,#3289);
#3287=VECTOR('',#10167,0.275);
#3288=VECTOR('',#10172,0.265);
#3289=VECTOR('',#10181,0.5);
#3529=CIRCLE('',#8265,0.285);
#3530=CIRCLE('',#8266,0.265);
#3531=CIRCLE('',#8268,0.265);
#3532=CIRCLE('',#8270,0.5);
#3533=CIRCLE('',#8272,0.5);
#4083=VERTEX_POINT('',#12359);
#4084=VERTEX_POINT('',#12361);
#4085=VERTEX_POINT('',#12365);
#4086=VERTEX_POINT('',#12369);
#4087=VERTEX_POINT('',#12372);
#4951=EDGE_CURVE('',#4083,#4083,#3529,.T.);
#4952=EDGE_CURVE('',#4083,#4084,#2578,.T.);
#4953=EDGE_CURVE('',#4084,#4084,#3530,.T.);
#4954=EDGE_CURVE('',#4084,#4085,#2579,.T.);
#4955=EDGE_CURVE('',#4085,#4085,#3531,.T.);
#4956=EDGE_CURVE('',#4086,#4086,#3532,.T.);
#4957=EDGE_CURVE('',#4086,#4087,#2580,.T.);
#4958=EDGE_CURVE('',#4087,#4087,#3533,.T.);
#6657=ORIENTED_EDGE('',*,*,#4951,.T.);
#6658=ORIENTED_EDGE('',*,*,#4952,.T.);
#6659=ORIENTED_EDGE('',*,*,#4953,.T.);
#6660=ORIENTED_EDGE('',*,*,#4952,.F.);
#6661=ORIENTED_EDGE('',*,*,#4953,.F.);
#6662=ORIENTED_EDGE('',*,*,#4954,.T.);
#6663=ORIENTED_EDGE('',*,*,#4955,.T.);
#6664=ORIENTED_EDGE('',*,*,#4954,.F.);
#6665=ORIENTED_EDGE('',*,*,#4956,.T.);
#6666=ORIENTED_EDGE('',*,*,#4951,.F.);
#6667=ORIENTED_EDGE('',*,*,#4956,.F.);
#6668=ORIENTED_EDGE('',*,*,#4957,.T.);
#6669=ORIENTED_EDGE('',*,*,#4958,.T.);
#6670=ORIENTED_EDGE('',*,*,#4957,.F.);
#6671=ORIENTED_EDGE('',*,*,#4958,.F.);
#6672=ORIENTED_EDGE('',*,*,#4955,.F.);
#6962=CYLINDRICAL_SURFACE('',#8267,0.265);
#6963=CYLINDRICAL_SURFACE('',#8271,0.5);
#7299=ADVANCED_FACE('',(#1373),#505,.F.);
#7300=ADVANCED_FACE('',(#1374),#6962,.F.);
#7301=ADVANCED_FACE('',(#1375,#755),#1009,.T.);
#7302=ADVANCED_FACE('',(#1376),#6963,.T.);
#7303=ADVANCED_FACE('',(#1377,#756),#1010,.F.);
#7390=CLOSED_SHELL('',(#7299,#7300,#7301,#7302,#7303));
#8263=AXIS2_PLACEMENT_3D('',#12357,#10161,#10162);
#8264=AXIS2_PLACEMENT_3D('',#12358,#10163,#10164);
#8265=AXIS2_PLACEMENT_3D('',#12360,#10165,#10166);
#8266=AXIS2_PLACEMENT_3D('',#12363,#10168,#10169);
#8267=AXIS2_PLACEMENT_3D('',#12364,#10170,#10171);
#8268=AXIS2_PLACEMENT_3D('',#12367,#10173,#10174);
#8269=AXIS2_PLACEMENT_3D('',#12368,#10175,#10176);
#8270=AXIS2_PLACEMENT_3D('',#12370,#10177,#10178);
#8271=AXIS2_PLACEMENT_3D('',#12371,#10179,#10180);
#8272=AXIS2_PLACEMENT_3D('',#12374,#10182,#10183);
#8273=AXIS2_PLACEMENT_3D('',#12375,#10184,#10185);
#10161=DIRECTION('axis',(0.,0.,1.));
#10162=DIRECTION('refdir',(1.,0.,0.));
#10163=DIRECTION('center_axis',(0.,1.,0.));
#10164=DIRECTION('ref_axis',(1.,0.,0.));
#10165=DIRECTION('center_axis',(0.,1.,0.));
#10166=DIRECTION('ref_axis',(1.,0.,0.));
#10167=DIRECTION('',(0.707106781186548,-0.707106781186547,-8.65956056235494E-17));
#10168=DIRECTION('center_axis',(0.,-1.,0.));
#10169=DIRECTION('ref_axis',(1.,0.,0.));
#10170=DIRECTION('center_axis',(0.,1.,0.));
#10171=DIRECTION('ref_axis',(1.,0.,0.));
#10172=DIRECTION('',(0.,-1.,0.));
#10173=DIRECTION('center_axis',(0.,-1.,0.));
#10174=DIRECTION('ref_axis',(1.,0.,0.));
#10175=DIRECTION('center_axis',(0.,1.,0.));
#10176=DIRECTION('ref_axis',(1.,0.,0.));
#10177=DIRECTION('center_axis',(0.,1.,0.));
#10178=DIRECTION('ref_axis',(1.,0.,0.));
#10179=DIRECTION('center_axis',(0.,1.,0.));
#10180=DIRECTION('ref_axis',(1.,0.,0.));
#10181=DIRECTION('',(0.,-1.,0.));
#10182=DIRECTION('center_axis',(0.,1.,0.));
#10183=DIRECTION('ref_axis',(1.,0.,0.));
#10184=DIRECTION('center_axis',(0.,1.,0.));
#10185=DIRECTION('ref_axis',(1.,0.,0.));
#12357=CARTESIAN_POINT('',(0.,0.,0.));
#12358=CARTESIAN_POINT('Origin',(0.,0.09,0.));
#12359=CARTESIAN_POINT('',(-0.285,0.1,3.49024337756996E-17));
#12360=CARTESIAN_POINT('Origin',(0.,0.1,0.));
#12361=CARTESIAN_POINT('',(-0.265,0.08,-3.24531401774049E-17));
#12362=CARTESIAN_POINT('',(-0.275,0.09,3.36777869765522E-17));
#12363=CARTESIAN_POINT('Origin',(0.,0.08,0.));
#12364=CARTESIAN_POINT('Origin',(0.,0.,0.));
#12365=CARTESIAN_POINT('',(-0.265,0.,3.24531401774049E-17));
#12366=CARTESIAN_POINT('',(-0.265,0.,3.24531401774049E-17));
#12367=CARTESIAN_POINT('Origin',(0.,0.,0.));
#12368=CARTESIAN_POINT('Origin',(0.,0.1,0.));
#12369=CARTESIAN_POINT('',(-0.5,0.1,6.12323399573677E-17));
#12370=CARTESIAN_POINT('Origin',(0.,0.1,0.));
#12371=CARTESIAN_POINT('Origin',(0.,0.,0.));
#12372=CARTESIAN_POINT('',(-0.5,0.,6.12323399573677E-17));
#12373=CARTESIAN_POINT('',(-0.5,0.,6.12323399573677E-17));
#12374=CARTESIAN_POINT('Origin',(0.,0.,0.));
#12375=CARTESIAN_POINT('Origin',(0.,0.,0.));
#12762=UNCERTAINTY_MEASURE_WITH_UNIT(LENGTH_MEASURE(0.001),#12805,
'DISTANCE_ACCURACY_VALUE',
'Maximum model space distance between geometric entities at asserted c
onnectivities');
#12768=UNCERTAINTY_MEASURE_WITH_UNIT(LENGTH_MEASURE(0.001),#12805,
'DISTANCE_ACCURACY_VALUE',
'Maximum model space distance between geometric entities at asserted c
onnectivities');
#12798=(
GEOMETRIC_REPRESENTATION_CONTEXT(3)
GLOBAL_UNCERTAINTY_ASSIGNED_CONTEXT((#12762))
GLOBAL_UNIT_ASSIGNED_CONTEXT((#12805,#12807,#12808))
REPRESENTATION_CONTEXT('','3D')
);
#12804=(
GEOMETRIC_REPRESENTATION_CONTEXT(3)
GLOBAL_UNCERTAINTY_ASSIGNED_CONTEXT((#12768))
GLOBAL_UNIT_ASSIGNED_CONTEXT((#12805,#12807,#12808))
REPRESENTATION_CONTEXT('','3D')
);
#12805=(
LENGTH_UNIT()
NAMED_UNIT(*)
SI_UNIT(.CENTI.,.METRE.)
);
#12807=(
NAMED_UNIT(*)
PLANE_ANGLE_UNIT()
SI_UNIT($,.RADIAN.)
);
#12808=(
NAMED_UNIT(*)
SI_UNIT($,.STERADIAN.)
SOLID_ANGLE_UNIT()
);
#12838=SHAPE_DEFINITION_REPRESENTATION(#12876,#13028);
#12876=PRODUCT_DEFINITION_SHAPE('',$,#13064);
#13028=SHAPE_REPRESENTATION('',(#8263),#12798);
#13034=PRODUCT_DEFINITION_CONTEXT('part definition',#13141,'design');
#13064=PRODUCT_DEFINITION('Flat Washer - M5','Flat Washer - M5',#13099,
#13034);
#13099=PRODUCT_DEFINITION_FORMATION('',$,#13172);
#13141=APPLICATION_CONTEXT(
'Core Data for Automotive Mechanical Design Process');
#13142=PRODUCT_CONTEXT('part definition',#13141,'mechanical');
#13172=PRODUCT('Flat Washer - M5','Flat Washer - M5','Flat Washer - M5',
(#13142));
#13248=COLOUR_RGB('Black',0.12,0.14,0.17);
#13249=FILL_AREA_STYLE_COLOUR('',#13248);
#13250=FILL_AREA_STYLE('',(#13249));
#13251=SURFACE_STYLE_FILL_AREA(#13250);
#13252=SURFACE_SIDE_STYLE('',(#13251));
#13253=SURFACE_STYLE_USAGE(.BOTH.,#13252);
#13254=PRESENTATION_STYLE_ASSIGNMENT((#13253));
ENDSEC;
END-ISO-10303-21;
